ISO-10303-21;
HEADER;
FILE_DESCRIPTION (('STEP AP214'),
    '1' );
FILE_NAME ('Pivot Pin Rivet.step',
    '2026-10-09T15:01:35',
    ( '' ),
    ( '' ),
    'SwSTEP 2.0',
    'SolidWorks 2026',
    '' );
FILE_SCHEMA (( 'AUTOMOTIVE_DESIGN' ));
ENDSEC;

DATA;
#48=AXIS2_PLACEMENT_3D ( 'NONE', #1305, #1866, #2469 ) ;
#56=VECTOR ( 'NONE', #5489, 1000.000000000000000 ) ;
#82=DIRECTION ( 'NONE',  ( -0.9721221936972339606, -0.2344748185227520099, 0.000000000000000000 ) ) ;
#97=ORIENTED_EDGE ( 'NONE', *, *, #2305, .F. ) ;
#108=DIRECTION ( 'NONE',  ( 0.2344748185227520099, -0.9721221936972339606, 0.000000000000000000 ) ) ;
#110=DIRECTION ( 'NONE',  ( -0.9721221936972339606, -0.2344748185227520099, 0.000000000000000000 ) ) ;
#126=DIRECTION ( 'NONE',  ( -0.2344748185227520376, 0.9721221936972340716, 0.000000000000000000 ) ) ;
#132=VECTOR ( 'NONE', #4275, 1000.000000000000000 ) ;
#134=CARTESIAN_POINT ( 'NONE',  ( -4.860610968486169803, -1.172374092613760022, 3.500000000000000000 ) ) ;
#141=( NAMED_UNIT ( * ) SI_UNIT ( $, .STERADIAN. ) SOLID_ANGLE_UNIT ( ) );
#143=DIRECTION ( 'NONE',  ( -0.9721221936972339606, -0.2344748185227520099, 0.000000000000000000 ) ) ;
#152=CARTESIAN_POINT ( 'NONE',  ( 0.000000000000000000, 0.000000000000000000, 2.544444444444450060 ) ) ;
#181=VERTEX_POINT ( 'NONE', #5749 ) ;
#186=CARTESIAN_POINT ( 'NONE',  ( 3.888488774788935842, 0.9378992740910084835, 3.000000000000000000 ) ) ;
#218=ORIENTED_EDGE ( 'NONE', *, *, #3975, .F. ) ;
#229=( NAMED_UNIT ( * ) SI_UNIT ( $, .STERADIAN. ) SOLID_ANGLE_UNIT ( ) );
#284=AXIS2_PLACEMENT_3D ( 'NONE', #2458, #4271, #126 ) ;
#355=ORIENTED_EDGE ( 'NONE', *, *, #4403, .T. ) ;
#389=DIRECTION ( 'NONE',  ( 0.000000000000000000, 0.000000000000000000, -1.000000000000000000 ) ) ;
#413=FACE_OUTER_BOUND ( 'NONE', #4875, .T. ) ;
#443=DIRECTION ( 'NONE',  ( 0.000000000000000000, 0.000000000000000000, 1.000000000000000000 ) ) ;
#483=FILL_AREA_STYLE_COLOUR ( '', #634 ) ;
#514=CIRCLE ( 'NONE', #4481, 5.000000000000000000 ) ;
#542=EDGE_CURVE ( 'NONE', #1973, #3934, #514, .T. ) ;
#579=EDGE_CURVE ( 'NONE', #7422, #1643, #2427, .T. ) ;
#611=EDGE_LOOP ( 'NONE', ( #6371, #3553, #1345 ) ) ;
#634=COLOUR_RGB ( '', 0.66274510, 0.83137255, 0.94901961) ;
#678=CARTESIAN_POINT ( 'NONE',  ( 0.000000000000000000, 0.000000000000000000, 2.544444444444450060 ) ) ;
#751=AXIS2_PLACEMENT_3D ( 'NONE', #5959, #3597, #6467 ) ;
#757=PRODUCT_DEFINITION_FORMATION_WITH_SPECIFIED_SOURCE ( 'ANY', '', #4771, .NOT_KNOWN. ) ;
#769=LINE ( 'NONE', #2532, #132 ) ;
#771=EDGE_LOOP ( 'NONE', ( #5192, #1574, #5528, #7020, #5156 ) ) ;
#792=ORIENTED_EDGE ( 'NONE', *, *, #6202, .T. ) ;
#812=CARTESIAN_POINT ( 'NONE',  ( 3.888488774788935842, 0.9378992740910084835, -17.67054229618195293 ) ) ;
#835=CARTESIAN_POINT ( 'NONE',  ( 1.172374092613760688, -4.860610968486169803, 3.500000000000000000 ) ) ;
#942=EDGE_CURVE ( 'NONE', #3934, #6950, #6758, .T. ) ;
#951=AXIS2_PLACEMENT_3D ( 'NONE', #2596, #2632, #3683 ) ;
#955=AXIS2_PLACEMENT_3D ( 'NONE', #1918, #6091, #7082 ) ;
#1126=CARTESIAN_POINT ( 'NONE',  ( 1.172374092613760022, -4.860610968486169803, -3.500000000000000000 ) ) ;
#1143=VERTEX_POINT ( 'NONE', #186 ) ;
#1245=( GEOMETRIC_REPRESENTATION_CONTEXT ( 3 ) GLOBAL_UNCERTAINTY_ASSIGNED_CONTEXT ( ( #2459 ) ) GLOBAL_UNIT_ASSIGNED_CONTEXT ( ( #1246, #4176, #141 ) ) REPRESENTATION_CONTEXT ( 'NONE', 'WORKASPACE' ) );
#1246=( LENGTH_UNIT ( ) NAMED_UNIT ( * ) SI_UNIT ( .MILLI., .METRE. ) );
#1278=EDGE_LOOP ( 'NONE', ( #3386, #355, #6802 ) ) ;
#1292=CARTESIAN_POINT ( 'NONE',  ( -4.860610968486169803, -1.172374092613760022, 3.000000000000000000 ) ) ;
#1305=CARTESIAN_POINT ( 'NONE',  ( 0.000000000000000000, 0.000000000000000000, -17.67054229618195293 ) ) ;
#1345=ORIENTED_EDGE ( 'NONE', *, *, #579, .F. ) ;
#1401=FACE_OUTER_BOUND ( 'NONE', #771, .T. ) ;
#1402=CARTESIAN_POINT ( 'NONE',  ( 0.000000000000000000, 0.000000000000000000, -3.000000000000000000 ) ) ;
#1419=CARTESIAN_POINT ( 'NONE',  ( 0.000000000000000000, 0.000000000000000000, 3.000000000000000000 ) ) ;
#1503=CARTESIAN_POINT ( 'NONE',  ( 0.000000000000000000, 0.000000000000000000, -3.000000000000000000 ) ) ;
#1574=ORIENTED_EDGE ( 'NONE', *, *, #6150, .T. ) ;
#1643=VERTEX_POINT ( 'NONE', #1967 ) ;
#1664=ORIENTED_EDGE ( 'NONE', *, *, #2730, .T. ) ;
#1670=ADVANCED_FACE ( 'NONE', ( #5270 ), #5407, .T. ) ;
#1690=CARTESIAN_POINT ( 'NONE',  ( -3.888488774788935842, -0.9378992740910081505, 3.000000000000000000 ) ) ;
#1691=CARTESIAN_POINT ( 'NONE',  ( 0.000000000000000000, 0.000000000000000000, -3.500000000000000000 ) ) ;
#1702=DIRECTION ( 'NONE',  ( -0.9721221936972339606, -0.2344748185227520099, 0.000000000000000000 ) ) ;
#1710=DIRECTION ( 'NONE',  ( -0.9721221936972339606, -0.2344748185227520376, 0.000000000000000000 ) ) ;
#1735=DIRECTION ( 'NONE',  ( -0.9721221936972339606, -0.2344748185227520099, 0.000000000000000000 ) ) ;
#1746=CYLINDRICAL_SURFACE ( 'NONE', #4980, 5.000000000000000000 ) ;
#1753=CARTESIAN_POINT ( 'NONE',  ( -4.860610968486169803, -1.172374092613760022, -3.500000000000000000 ) ) ;
#1805=AXIS2_PLACEMENT_3D ( 'NONE', #7039, #5280, #82 ) ;
#1832=FACE_OUTER_BOUND ( 'NONE', #611, .T. ) ;
#1833=STYLED_ITEM ( 'NONE', ( #4522 ), #2417 ) ;
#1853=AXIS2_PLACEMENT_3D ( 'NONE', #678, #5914, #108 ) ;
#1865=VERTEX_POINT ( 'NONE', #2114 ) ;
#1866=DIRECTION ( 'NONE',  ( 0.000000000000000000, 0.000000000000000000, -1.000000000000000000 ) ) ;
#1869=CARTESIAN_POINT ( 'NONE',  ( 4.860610968486169803, 1.172374092613760688, -3.500000000000000000 ) ) ;
#1903=SPHERICAL_SURFACE ( 'NONE', #1853, 7.844444444444450326 ) ;
#1918=CARTESIAN_POINT ( 'NONE',  ( 0.000000000000000000, 0.000000000000000000, -3.000000000000000000 ) ) ;
#1960=VECTOR ( 'NONE', #389, 1000.000000000000000 ) ;
#1966=AXIS2_PLACEMENT_3D ( 'NONE', #6502, #2993, #143 ) ;
#1967=CARTESIAN_POINT ( 'NONE',  ( 4.860610968486169803, 1.172374092613760688, 3.500000000000000000 ) ) ;
#1973=VERTEX_POINT ( 'NONE', #1753 ) ;
#2005=DIRECTION ( 'NONE',  ( 0.000000000000000000, 0.000000000000000000, -1.000000000000000000 ) ) ;
#2011=PRODUCT_CONTEXT ( 'NONE', #4578, 'mechanical' ) ;
#2013=DIRECTION ( 'NONE',  ( 0.000000000000000000, 0.000000000000000000, -1.000000000000000000 ) ) ;
#2041=DIRECTION ( 'NONE',  ( 0.9721221936972340716, 0.2344748185227520376, 0.000000000000000000 ) ) ;
#2050=CARTESIAN_POINT ( 'NONE',  ( 0.000000000000000000, 0.000000000000000000, -3.000000000000000000 ) ) ;
#2097=ADVANCED_FACE ( 'NONE', ( #1401 ), #6669, .T. ) ;
#2114=CARTESIAN_POINT ( 'NONE',  ( 3.888488774788935842, 0.9378992740910084835, -3.000000000000000000 ) ) ;
#2136=SHAPE_REPRESENTATION ( 'Pivot Pin Rivet', ( #751 ), #1245 ) ;
#2143=LINE ( 'NONE', #3280, #1960 ) ;
#2171=LINE ( 'NONE', #3951, #5298 ) ;
#2191=AXIS2_PLACEMENT_3D ( 'NONE', #5067, #2005, #1710 ) ;
#2209=CARTESIAN_POINT ( 'NONE',  ( 0.000000000000000000, 0.000000000000000000, 3.500000000000000000 ) ) ;
#2213=ORIENTED_EDGE ( 'NONE', *, *, #4137, .T. ) ;
#2218=AXIS2_PLACEMENT_3D ( 'NONE', #1419, #4818, #3709 ) ;
#2244=SHAPE_DEFINITION_REPRESENTATION ( #4288, #2136 ) ;
#2262=DIRECTION ( 'NONE',  ( -0.9721221936972339606, -0.2344748185227521209, -0.000000000000000000 ) ) ;
#2278=CIRCLE ( 'NONE', #6485, 5.000000000000000000 ) ;
#2305=EDGE_CURVE ( 'NONE', #7415, #4629, #5140, .T. ) ;
#2359=ORIENTED_EDGE ( 'NONE', *, *, #5447, .F. ) ;
#2391=CARTESIAN_POINT ( 'NONE',  ( 0.000000000000000000, 0.000000000000000000, 3.000000000000000000 ) ) ;
#2395=VERTEX_POINT ( 'NONE', #1292 ) ;
#2397=DIRECTION ( 'NONE',  ( 0.000000000000000000, 0.000000000000000000, -1.000000000000000000 ) ) ;
#2409=AXIS2_PLACEMENT_3D ( 'NONE', #5567, #3850, #443 ) ;
#2416=FACE_BOUND ( 'NONE', #6516, .T. ) ;
#2417=MANIFOLD_SOLID_BREP ( 'NONE', #3133 ) ;
#2427=CIRCLE ( 'NONE', #2780, 5.000000000000000000 ) ;
#2437=CARTESIAN_POINT ( 'NONE',  ( 0.000000000000000000, 0.000000000000000000, 3.000000000000000000 ) ) ;
#2458=CARTESIAN_POINT ( 'NONE',  ( -0.9378992740910081505, 3.888488774788935842, 3.000000000000000000 ) ) ;
#2459=UNCERTAINTY_MEASURE_WITH_UNIT (LENGTH_MEASURE( 1.000000000000000082E-05 ), #1246, 'distance_accuracy_value', 'NONE');
#2469=DIRECTION ( 'NONE',  ( -0.9721221936972339606, -0.2344748185227520376, 0.000000000000000000 ) ) ;
#2476=ORIENTED_EDGE ( 'NONE', *, *, #6115, .T. ) ;
#2497=CARTESIAN_POINT ( 'NONE',  ( 4.860610968486169803, 1.172374092613760688, 3.000000000000000000 ) ) ;
#2527=AXIS2_PLACEMENT_3D ( 'NONE', #6319, #5642, #3407 ) ;
#2532=CARTESIAN_POINT ( 'NONE',  ( 4.860610968486169803, 1.172374092613760688, -17.67054229618195293 ) ) ;
#2590=DIRECTION ( 'NONE',  ( -0.9721221936972339606, -0.2344748185227520376, 0.000000000000000000 ) ) ;
#2596=CARTESIAN_POINT ( 'NONE',  ( 0.000000000000000000, 0.000000000000000000, 3.500000000000000000 ) ) ;
#2605=EDGE_CURVE ( 'NONE', #1143, #7415, #5328, .T. ) ;
#2632=DIRECTION ( 'NONE',  ( 0.000000000000000000, 0.000000000000000000, -1.000000000000000000 ) ) ;
#2651=DIRECTION ( 'NONE',  ( -0.9721221936972339606, -0.2344748185227520099, 0.000000000000000000 ) ) ;
#2692=FACE_BOUND ( 'NONE', #5121, .T. ) ;
#2713=VERTEX_POINT ( 'NONE', #134 ) ;
#2730=EDGE_CURVE ( 'NONE', #2713, #7422, #3272, .T. ) ;
#2752=CYLINDRICAL_SURFACE ( 'NONE', #2191, 4.000000000000000000 ) ;
#2780=AXIS2_PLACEMENT_3D ( 'NONE', #6472, #5030, #2651 ) ;
#2803=AXIS2_PLACEMENT_3D ( 'NONE', #2960, #6881, #5302 ) ;
#2838=EDGE_LOOP ( 'NONE', ( #2476, #2213 ) ) ;
#2855=VERTEX_POINT ( 'NONE', #835 ) ;
#2906=( GEOMETRIC_REPRESENTATION_CONTEXT ( 3 ) GLOBAL_UNCERTAINTY_ASSIGNED_CONTEXT ( ( #5327 ) ) GLOBAL_UNIT_ASSIGNED_CONTEXT ( ( #3858, #3902, #229 ) ) REPRESENTATION_CONTEXT ( 'NONE', 'WORKASPACE' ) );
#2919=ADVANCED_FACE ( 'NONE', ( #2692, #3810 ), #3288, .T. ) ;
#2940=DIRECTION ( 'NONE',  ( 0.2344748185227520099, -0.9721221936972339606, 0.000000000000000000 ) ) ;
#2960=CARTESIAN_POINT ( 'NONE',  ( 0.000000000000000000, 0.000000000000000000, -2.544444444444450060 ) ) ;
#2993=DIRECTION ( 'NONE',  ( 0.000000000000000000, 0.000000000000000000, -1.000000000000000000 ) ) ;
#2997=ADVANCED_FACE ( 'NONE', ( #3323 ), #2752, .T. ) ;
#3039=DIRECTION ( 'NONE',  ( 0.000000000000000000, 0.000000000000000000, -1.000000000000000000 ) ) ;
#3047=DIRECTION ( 'NONE',  ( 0.000000000000000000, 0.000000000000000000, 1.000000000000000000 ) ) ;
#3086=DIRECTION ( 'NONE',  ( 0.000000000000000000, 0.000000000000000000, -1.000000000000000000 ) ) ;
#3126=ORIENTED_EDGE ( 'NONE', *, *, #6164, .T. ) ;
#3133=CLOSED_SHELL ( 'NONE', ( #3605, #2097, #2919, #1670, #3189, #4897, #6788, #6935, #5411, #2997, #3572, #6105 ) ) ;
#3136=ORIENTED_EDGE ( 'NONE', *, *, #3774, .T. ) ;
#3161=ORIENTED_EDGE ( 'NONE', *, *, #2605, .T. ) ;
#3189=ADVANCED_FACE ( 'NONE', ( #2416, #7016 ), #4692, .T. ) ;
#3214=ORIENTED_EDGE ( 'NONE', *, *, #4171, .F. ) ;
#3219=EDGE_CURVE ( 'NONE', #181, #4378, #3761, .T. ) ;
#3272=CIRCLE ( 'NONE', #4128, 5.000000000000000000 ) ;
#3280=CARTESIAN_POINT ( 'NONE',  ( -4.860610968486169803, -1.172374092613760022, -17.67054229618195293 ) ) ;
#3288=PLANE ( 'NONE',  #4492 ) ;
#3302=SPHERICAL_SURFACE ( 'NONE', #6886, 7.844444444444450326 ) ;
#3310=ORIENTED_EDGE ( 'NONE', *, *, #6150, .F. ) ;
#3323=FACE_OUTER_BOUND ( 'NONE', #5725, .T. ) ;
#3328=FACE_OUTER_BOUND ( 'NONE', #3791, .T. ) ;
#3358=ORIENTED_EDGE ( 'NONE', *, *, #6202, .F. ) ;
#3386=ORIENTED_EDGE ( 'NONE', *, *, #542, .T. ) ;
#3391=CARTESIAN_POINT ( 'NONE',  ( 0.000000000000000000, 0.000000000000000000, -17.67054229618195293 ) ) ;
#3407=DIRECTION ( 'NONE',  ( -0.9721221936972339606, -0.2344748185227520099, 0.000000000000000000 ) ) ;
#3408=AXIS2_PLACEMENT_3D ( 'NONE', #1402, #3086, #5370 ) ;
#3514=AXIS2_PLACEMENT_3D ( 'NONE', #1691, #2397, #1735 ) ;
#3537=FACE_OUTER_BOUND ( 'NONE', #1278, .T. ) ;
#3538=AXIS2_PLACEMENT_3D ( 'NONE', #2437, #7037, #4364 ) ;
#3542=CIRCLE ( 'NONE', #2218, 4.000000000000000000 ) ;
#3553=ORIENTED_EDGE ( 'NONE', *, *, #3774, .F. ) ;
#3572=ADVANCED_FACE ( 'NONE', ( #6939 ), #1746, .T. ) ;
#3597=DIRECTION ( 'NONE',  ( 0.000000000000000000, 0.000000000000000000, 1.000000000000000000 ) ) ;
#3605=ADVANCED_FACE ( 'NONE', ( #5630 ), #4151, .T. ) ;
#3647=CIRCLE ( 'NONE', #4626, 5.000000000000000000 ) ;
#3683=DIRECTION ( 'NONE',  ( -0.9721221936972339606, -0.2344748185227520099, 0.000000000000000000 ) ) ;
#3688=LINE ( 'NONE', #5369, #56 ) ;
#3704=ORIENTED_EDGE ( 'NONE', *, *, #4171, .T. ) ;
#3709=DIRECTION ( 'NONE',  ( -0.9721221936972339606, -0.2344748185227520376, 0.000000000000000000 ) ) ;
#3740=ORIENTED_EDGE ( 'NONE', *, *, #942, .F. ) ;
#3761=CIRCLE ( 'NONE', #3408, 5.000000000000000000 ) ;
#3774=EDGE_CURVE ( 'NONE', #1643, #2855, #7199, .T. ) ;
#3791=EDGE_LOOP ( 'NONE', ( #218, #3136, #4884, #6213, #7408 ) ) ;
#3810=FACE_OUTER_BOUND ( 'NONE', #5861, .T. ) ;
#3839=CARTESIAN_POINT ( 'NONE',  ( 4.860610968486169803, 1.172374092613760688, -3.000000000000000000 ) ) ;
#3850=DIRECTION ( 'NONE',  ( -0.9721221936972339606, -0.2344748185227520099, 0.000000000000000000 ) ) ;
#3854=ORIENTED_EDGE ( 'NONE', *, *, #6239, .F. ) ;
#3858=( LENGTH_UNIT ( ) NAMED_UNIT ( * ) SI_UNIT ( .MILLI., .METRE. ) );
#3879=CARTESIAN_POINT ( 'NONE',  ( 0.000000000000000000, 0.000000000000000000, 2.544444444444450060 ) ) ;
#3902=( NAMED_UNIT ( * ) PLANE_ANGLE_UNIT ( ) SI_UNIT ( $, .RADIAN. ) );
#3934=VERTEX_POINT ( 'NONE', #4488 ) ;
#3941=DIRECTION ( 'NONE',  ( -0.2344748185227520099, 0.9721221936972339606, 0.000000000000000000 ) ) ;
#3951=CARTESIAN_POINT ( 'NONE',  ( 4.860610968486169803, 1.172374092613760688, -17.67054229618195293 ) ) ;
#3975=EDGE_CURVE ( 'NONE', #1643, #5210, #2171, .T. ) ;
#3983=EDGE_LOOP ( 'NONE', ( #5017, #6844, #7174 ) ) ;
#3994=VECTOR ( 'NONE', #6511, 1000.000000000000000 ) ;
#4016=ORIENTED_EDGE ( 'NONE', *, *, #3219, .F. ) ;
#4068=CARTESIAN_POINT ( 'NONE',  ( 0.000000000000000000, 0.000000000000000000, -3.500000000000000000 ) ) ;
#4128=AXIS2_PLACEMENT_3D ( 'NONE', #7090, #7029, #4201 ) ;
#4137=EDGE_CURVE ( 'NONE', #5210, #2395, #6376, .T. ) ;
#4151=SPHERICAL_SURFACE ( 'NONE', #5048, 7.844444444444450326 ) ;
#4152=EDGE_CURVE ( 'NONE', #6387, #1973, #2278, .T. ) ;
#4171=EDGE_CURVE ( 'NONE', #1865, #4629, #6850, .T. ) ;
#4176=( NAMED_UNIT ( * ) PLANE_ANGLE_UNIT ( ) SI_UNIT ( $, .RADIAN. ) );
#4181=DIRECTION ( 'NONE',  ( -0.9721221936972339606, -0.2344748185227520099, 0.000000000000000000 ) ) ;
#4201=DIRECTION ( 'NONE',  ( -0.9721221936972339606, -0.2344748185227520099, 0.000000000000000000 ) ) ;
#4245=EDGE_LOOP ( 'NONE', ( #6897, #4284, #7378, #2359, #1664 ) ) ;
#4249=DIRECTION ( 'NONE',  ( 0.000000000000000000, 0.000000000000000000, -1.000000000000000000 ) ) ;
#4256=PRODUCT_DEFINITION ( 'UNKNOWN', '', #757, #6672 ) ;
#4271=DIRECTION ( 'NONE',  ( 0.000000000000000000, 0.000000000000000000, -1.000000000000000000 ) ) ;
#4275=DIRECTION ( 'NONE',  ( 0.000000000000000000, 0.000000000000000000, -1.000000000000000000 ) ) ;
#4284=ORIENTED_EDGE ( 'NONE', *, *, #3975, .T. ) ;
#4288=PRODUCT_DEFINITION_SHAPE ( 'NONE', 'NONE',  #4256 ) ;
#4364=DIRECTION ( 'NONE',  ( -0.9721221936972339606, -0.2344748185227520099, 0.000000000000000000 ) ) ;
#4378=VERTEX_POINT ( 'NONE', #3839 ) ;
#4382=CARTESIAN_POINT ( 'NONE',  ( 0.000000000000000000, 0.000000000000000000, -17.67054229618195293 ) ) ;
#4390=ORIENTED_EDGE ( 'NONE', *, *, #4909, .T. ) ;
#4403=EDGE_CURVE ( 'NONE', #3934, #6387, #6613, .T. ) ;
#4469=ORIENTED_EDGE ( 'NONE', *, *, #2305, .T. ) ;
#4474=FILL_AREA_STYLE ('',( #483 ) ) ;
#4481=AXIS2_PLACEMENT_3D ( 'NONE', #5606, #6062, #4181 ) ;
#4488=CARTESIAN_POINT ( 'NONE',  ( -1.172374092613760688, 4.860610968486169803, -3.500000000000000000 ) ) ;
#4492=AXIS2_PLACEMENT_3D ( 'NONE', #5530, #4923, #2041 ) ;
#4517=VECTOR ( 'NONE', #2013, 1000.000000000000000 ) ;
#4522=PRESENTATION_STYLE_ASSIGNMENT (( #6585 ) ) ;
#4578=APPLICATION_CONTEXT ( 'automotive_design' ) ;
#4626=AXIS2_PLACEMENT_3D ( 'NONE', #2209, #5650, #6840 ) ;
#4629=VERTEX_POINT ( 'NONE', #5550 ) ;
#4668=ORIENTED_EDGE ( 'NONE', *, *, #2730, .F. ) ;
#4692=PLANE ( 'NONE',  #284 ) ;
#4701=DIRECTION ( 'NONE',  ( 0.000000000000000000, 0.000000000000000000, -1.000000000000000000 ) ) ;
#4771=PRODUCT ( 'Pivot Pin Rivet', 'Pivot Pin Rivet', '', ( #2011 ) ) ;
#4818=DIRECTION ( 'NONE',  ( 0.000000000000000000, 0.000000000000000000, -1.000000000000000000 ) ) ;
#4861=AXIS2_PLACEMENT_3D ( 'NONE', #5022, #6710, #7421 ) ;
#4875=EDGE_LOOP ( 'NONE', ( #5037, #4390, #4668 ) ) ;
#4884=ORIENTED_EDGE ( 'NONE', *, *, #6734, .T. ) ;
#4897=ADVANCED_FACE ( 'NONE', ( #3328 ), #5608, .T. ) ;
#4909=EDGE_CURVE ( 'NONE', #2855, #7422, #6737, .T. ) ;
#4923=DIRECTION ( 'NONE',  ( 0.000000000000000000, -0.000000000000000000, 1.000000000000000000 ) ) ;
#4980=AXIS2_PLACEMENT_3D ( 'NONE', #3391, #5215, #1702 ) ;
#5007=DIRECTION ( 'NONE',  ( 0.000000000000000000, -0.000000000000000000, 1.000000000000000000 ) ) ;
#5017=ORIENTED_EDGE ( 'NONE', *, *, #4403, .F. ) ;
#5022=CARTESIAN_POINT ( 'NONE',  ( 0.000000000000000000, 0.000000000000000000, -17.67054229618195293 ) ) ;
#5030=DIRECTION ( 'NONE',  ( 0.000000000000000000, 0.000000000000000000, -1.000000000000000000 ) ) ;
#5037=ORIENTED_EDGE ( 'NONE', *, *, #6734, .F. ) ;
#5048=AXIS2_PLACEMENT_3D ( 'NONE', #152, #3047, #2940 ) ;
#5067=CARTESIAN_POINT ( 'NONE',  ( 0.000000000000000000, 0.000000000000000000, -17.67054229618195293 ) ) ;
#5121=EDGE_LOOP ( 'NONE', ( #3126, #3704 ) ) ;
#5140=LINE ( 'NONE', #6411, #3994 ) ;
#5156=ORIENTED_EDGE ( 'NONE', *, *, #6114, .F. ) ;
#5192=ORIENTED_EDGE ( 'NONE', *, *, #5198, .F. ) ;
#5198=EDGE_CURVE ( 'NONE', #4378, #6950, #769, .T. ) ;
#5210=VERTEX_POINT ( 'NONE', #2497 ) ;
#5215=DIRECTION ( 'NONE',  ( 0.000000000000000000, 0.000000000000000000, -1.000000000000000000 ) ) ;
#5270=FACE_OUTER_BOUND ( 'NONE', #6035, .T. ) ;
#5280=DIRECTION ( 'NONE',  ( 0.000000000000000000, 0.000000000000000000, -1.000000000000000000 ) ) ;
#5298=VECTOR ( 'NONE', #7376, 1000.000000000000000 ) ;
#5302=DIRECTION ( 'NONE',  ( -0.2344748185227520099, 0.9721221936972339606, 0.000000000000000000 ) ) ;
#5312=ADVANCED_BREP_SHAPE_REPRESENTATION ( '', ( #2417, #751 ), #1245 ) ;
#5327=UNCERTAINTY_MEASURE_WITH_UNIT (LENGTH_MEASURE( 1.000000000000000082E-05 ), #3858, 'distance_accuracy_value', 'NONE');
#5328=CIRCLE ( 'NONE', #6418, 4.000000000000000000 ) ;
#5369=CARTESIAN_POINT ( 'NONE',  ( -4.860610968486169803, -1.172374092613760022, -17.67054229618195293 ) ) ;
#5370=DIRECTION ( 'NONE',  ( -0.9721221936972339606, -0.2344748185227520099, 0.000000000000000000 ) ) ;
#5387=DIRECTION ( 'NONE',  ( -0.9721221936972339606, -0.2344748185227520099, 0.000000000000000000 ) ) ;
#5392=SURFACE_SIDE_STYLE ('',( #6176 ) ) ;
#5407=CYLINDRICAL_SURFACE ( 'NONE', #48, 4.000000000000000000 ) ;
#5411=ADVANCED_FACE ( 'NONE', ( #6677 ), #6199, .T. ) ;
#5419=SHAPE_REPRESENTATION_RELATIONSHIP ( 'NONE' , 'NONE' ,  #2136, #5312 ) ;
#5437=DIRECTION ( 'NONE',  ( 0.000000000000000000, 0.000000000000000000, -1.000000000000000000 ) ) ;
#5447=EDGE_CURVE ( 'NONE', #2713, #2395, #2143, .T. ) ;
#5475=ORIENTED_EDGE ( 'NONE', *, *, #2605, .F. ) ;
#5485=AXIS2_PLACEMENT_3D ( 'NONE', #2050, #6578, #5387 ) ;
#5489=DIRECTION ( 'NONE',  ( 0.000000000000000000, 0.000000000000000000, -1.000000000000000000 ) ) ;
#5528=ORIENTED_EDGE ( 'NONE', *, *, #5702, .T. ) ;
#5530=CARTESIAN_POINT ( 'NONE',  ( -1.172374092613760022, 4.860610968486169803, -3.000000000000000000 ) ) ;
#5550=CARTESIAN_POINT ( 'NONE',  ( -3.888488774788935842, -0.9378992740910081505, -3.000000000000000000 ) ) ;
#5567=CARTESIAN_POINT ( 'NONE',  ( 0.000000000000000000, 0.000000000000000000, -2.544444444444450060 ) ) ;
#5606=CARTESIAN_POINT ( 'NONE',  ( 0.000000000000000000, 0.000000000000000000, -3.500000000000000000 ) ) ;
#5608=CYLINDRICAL_SURFACE ( 'NONE', #2527, 5.000000000000000000 ) ;
#5630=FACE_OUTER_BOUND ( 'NONE', #3983, .T. ) ;
#5642=DIRECTION ( 'NONE',  ( 0.000000000000000000, 0.000000000000000000, -1.000000000000000000 ) ) ;
#5650=DIRECTION ( 'NONE',  ( 0.000000000000000000, 0.000000000000000000, -1.000000000000000000 ) ) ;
#5702=EDGE_CURVE ( 'NONE', #181, #1973, #3688, .T. ) ;
#5725=EDGE_LOOP ( 'NONE', ( #6095, #792, #7307, #97 ) ) ;
#5733=SPHERICAL_SURFACE ( 'NONE', #2803, 7.844444444444450326 ) ;
#5749=CARTESIAN_POINT ( 'NONE',  ( -4.860610968486169803, -1.172374092613760022, -3.000000000000000000 ) ) ;
#5769=CARTESIAN_POINT ( 'NONE',  ( -1.172374092613760022, 4.860610968486169803, 3.500000000000000000 ) ) ;
#5861=EDGE_LOOP ( 'NONE', ( #4016, #3310 ) ) ;
#5914=DIRECTION ( 'NONE',  ( 0.000000000000000000, 0.000000000000000000, 1.000000000000000000 ) ) ;
#5959=CARTESIAN_POINT ( 'NONE',  ( 0.000000000000000000, 0.000000000000000000, 0.000000000000000000 ) ) ;
#6006=DIRECTION ( 'NONE',  ( -0.9721221936972339606, -0.2344748185227520099, 0.000000000000000000 ) ) ;
#6023=ORIENTED_EDGE ( 'NONE', *, *, #3219, .T. ) ;
#6031=AXIS2_PLACEMENT_3D ( 'NONE', #3879, #2262, #6858 ) ;
#6035=EDGE_LOOP ( 'NONE', ( #3358, #3161, #4469, #3214 ) ) ;
#6062=DIRECTION ( 'NONE',  ( 0.000000000000000000, 0.000000000000000000, -1.000000000000000000 ) ) ;
#6087=AXIS2_PLACEMENT_3D ( 'NONE', #1503, #4249, #2590 ) ;
#6091=DIRECTION ( 'NONE',  ( 0.000000000000000000, 0.000000000000000000, -1.000000000000000000 ) ) ;
#6095=ORIENTED_EDGE ( 'NONE', *, *, #6239, .T. ) ;
#6105=ADVANCED_FACE ( 'NONE', ( #3537 ), #1903, .T. ) ;
#6114=EDGE_CURVE ( 'NONE', #6950, #6387, #6546, .T. ) ;
#6115=EDGE_CURVE ( 'NONE', #2395, #5210, #7142, .T. ) ;
#6150=EDGE_CURVE ( 'NONE', #4378, #181, #7032, .T. ) ;
#6164=EDGE_CURVE ( 'NONE', #4629, #1865, #6438, .T. ) ;
#6176=SURFACE_STYLE_FILL_AREA ( #4474 ) ;
#6199=CYLINDRICAL_SURFACE ( 'NONE', #4861, 5.000000000000000000 ) ;
#6202=EDGE_CURVE ( 'NONE', #1143, #1865, #7178, .T. ) ;
#6213=ORIENTED_EDGE ( 'NONE', *, *, #5447, .T. ) ;
#6239=EDGE_CURVE ( 'NONE', #7415, #1143, #3542, .T. ) ;
#6319=CARTESIAN_POINT ( 'NONE',  ( 0.000000000000000000, 0.000000000000000000, -17.67054229618195293 ) ) ;
#6340=ORIENTED_EDGE ( 'NONE', *, *, #542, .F. ) ;
#6371=ORIENTED_EDGE ( 'NONE', *, *, #4909, .F. ) ;
#6376=CIRCLE ( 'NONE', #1805, 5.000000000000000000 ) ;
#6387=VERTEX_POINT ( 'NONE', #1126 ) ;
#6403=APPLICATION_CONTEXT ( 'automotive_design' ) ;
#6411=CARTESIAN_POINT ( 'NONE',  ( -3.888488774788935842, -0.9378992740910081505, -17.67054229618195293 ) ) ;
#6418=AXIS2_PLACEMENT_3D ( 'NONE', #2391, #4701, #6987 ) ;
#6438=CIRCLE ( 'NONE', #6087, 4.000000000000000000 ) ;
#6467=DIRECTION ( 'NONE',  ( 1.000000000000000000, 0.000000000000000000, 0.000000000000000000 ) ) ;
#6472=CARTESIAN_POINT ( 'NONE',  ( 0.000000000000000000, 0.000000000000000000, 3.500000000000000000 ) ) ;
#6485=AXIS2_PLACEMENT_3D ( 'NONE', #4068, #3039, #110 ) ;
#6499=ORIENTED_EDGE ( 'NONE', *, *, #5702, .F. ) ;
#6502=CARTESIAN_POINT ( 'NONE',  ( 0.000000000000000000, 0.000000000000000000, -3.500000000000000000 ) ) ;
#6511=DIRECTION ( 'NONE',  ( 0.000000000000000000, 0.000000000000000000, -1.000000000000000000 ) ) ;
#6516=EDGE_LOOP ( 'NONE', ( #3854, #5475 ) ) ;
#6517=MECHANICAL_DESIGN_GEOMETRIC_PRESENTATION_REPRESENTATION('',(#1833),#2906);
#6546=CIRCLE ( 'NONE', #1966, 5.000000000000000000 ) ;
#6578=DIRECTION ( 'NONE',  ( 0.000000000000000000, 0.000000000000000000, -1.000000000000000000 ) ) ;
#6585=SURFACE_STYLE_USAGE ( .BOTH. , #5392 ) ;
#6588=ORIENTED_EDGE ( 'NONE', *, *, #5198, .T. ) ;
#6613=CIRCLE ( 'NONE', #6031, 7.844444444444450326 ) ;
#6669=CYLINDRICAL_SURFACE ( 'NONE', #7349, 5.000000000000000000 ) ;
#6672=PRODUCT_DEFINITION_CONTEXT ( 'detailed design', #6403, 'design' ) ;
#6677=FACE_OUTER_BOUND ( 'NONE', #4245, .T. ) ;
#6694=CARTESIAN_POINT ( 'NONE',  ( 0.000000000000000000, 0.000000000000000000, -2.544444444444450060 ) ) ;
#6710=DIRECTION ( 'NONE',  ( 0.000000000000000000, 0.000000000000000000, -1.000000000000000000 ) ) ;
#6734=EDGE_CURVE ( 'NONE', #2855, #2713, #3647, .T. ) ;
#6737=CIRCLE ( 'NONE', #2409, 7.844444444444450326 ) ;
#6758=CIRCLE ( 'NONE', #3514, 5.000000000000000000 ) ;
#6788=ADVANCED_FACE ( 'NONE', ( #413 ), #3302, .T. ) ;
#6802=ORIENTED_EDGE ( 'NONE', *, *, #4152, .T. ) ;
#6840=DIRECTION ( 'NONE',  ( -0.9721221936972339606, -0.2344748185227520099, 0.000000000000000000 ) ) ;
#6844=ORIENTED_EDGE ( 'NONE', *, *, #942, .T. ) ;
#6850=CIRCLE ( 'NONE', #955, 4.000000000000000000 ) ;
#6858=DIRECTION ( 'NONE',  ( -0.2344748185227521209, 0.9721221936972339606, 0.000000000000000000 ) ) ;
#6881=DIRECTION ( 'NONE',  ( 0.000000000000000000, -0.000000000000000000, 1.000000000000000000 ) ) ;
#6886=AXIS2_PLACEMENT_3D ( 'NONE', #6694, #5007, #3941 ) ;
#6897=ORIENTED_EDGE ( 'NONE', *, *, #579, .T. ) ;
#6935=ADVANCED_FACE ( 'NONE', ( #1832 ), #5733, .T. ) ;
#6939=FACE_OUTER_BOUND ( 'NONE', #6957, .T. ) ;
#6950=VERTEX_POINT ( 'NONE', #1869 ) ;
#6957=EDGE_LOOP ( 'NONE', ( #6023, #6588, #3740, #6340, #6499 ) ) ;
#6987=DIRECTION ( 'NONE',  ( -0.9721221936972339606, -0.2344748185227520376, 0.000000000000000000 ) ) ;
#7016=FACE_OUTER_BOUND ( 'NONE', #2838, .T. ) ;
#7020=ORIENTED_EDGE ( 'NONE', *, *, #4152, .F. ) ;
#7029=DIRECTION ( 'NONE',  ( 0.000000000000000000, 0.000000000000000000, -1.000000000000000000 ) ) ;
#7032=CIRCLE ( 'NONE', #5485, 5.000000000000000000 ) ;
#7037=DIRECTION ( 'NONE',  ( 0.000000000000000000, 0.000000000000000000, -1.000000000000000000 ) ) ;
#7039=CARTESIAN_POINT ( 'NONE',  ( 0.000000000000000000, 0.000000000000000000, 3.000000000000000000 ) ) ;
#7082=DIRECTION ( 'NONE',  ( -0.9721221936972339606, -0.2344748185227520376, 0.000000000000000000 ) ) ;
#7090=CARTESIAN_POINT ( 'NONE',  ( 0.000000000000000000, 0.000000000000000000, 3.500000000000000000 ) ) ;
#7142=CIRCLE ( 'NONE', #3538, 5.000000000000000000 ) ;
#7174=ORIENTED_EDGE ( 'NONE', *, *, #6114, .T. ) ;
#7178=LINE ( 'NONE', #812, #4517 ) ;
#7199=CIRCLE ( 'NONE', #951, 5.000000000000000000 ) ;
#7307=ORIENTED_EDGE ( 'NONE', *, *, #6164, .F. ) ;
#7349=AXIS2_PLACEMENT_3D ( 'NONE', #4382, #5437, #6006 ) ;
#7376=DIRECTION ( 'NONE',  ( 0.000000000000000000, 0.000000000000000000, -1.000000000000000000 ) ) ;
#7378=ORIENTED_EDGE ( 'NONE', *, *, #6115, .F. ) ;
#7408=ORIENTED_EDGE ( 'NONE', *, *, #4137, .F. ) ;
#7415=VERTEX_POINT ( 'NONE', #1690 ) ;
#7421=DIRECTION ( 'NONE',  ( -0.9721221936972339606, -0.2344748185227520099, 0.000000000000000000 ) ) ;
#7422=VERTEX_POINT ( 'NONE', #5769 ) ;
ENDSEC;
END-ISO-10303-21;
